ISO-10303-21;
HEADER;
FILE_DESCRIPTION (('STEP AP203'),
    '1' );
FILE_NAME ('1602p_c_19.step',
    '2026-10-31T14:11:27',
    ( '' ),
    ( '' ),
    'SwSTEP 2.0',
    'SolidWorks 2024',
    '' );
FILE_SCHEMA (( 'AUTOMOTIVE_DESIGN' ));
ENDSEC;

DATA;
#26=VECTOR ( 'NONE', #14901, 1000.000000000000000 ) ;
#65=ADVANCED_FACE ( 'NONE', ( #10736 ), #4781, .T. ) ;
#180=ORIENTED_EDGE ( 'NONE', *, *, #10830, .F. ) ;
#246=ADVANCED_FACE ( 'NONE', ( #18435 ), #4045, .T. ) ;
#260=CARTESIAN_POINT ( 'NONE',  ( -19.99999998565371229, 20.20208919256890212, -8.499999999995543121 ) ) ;
#320=CARTESIAN_POINT ( 'NONE',  ( -20.00000000397420052, 22.95208919256889857, -6.499999999995379696 ) ) ;
#402=CARTESIAN_POINT ( 'NONE',  ( -20.00000000397469790, 22.95208919256889857, -8.499999999995548450 ) ) ;
#415=DIRECTION ( 'NONE',  ( 1.000000000000000000, 0.000000000000000000, 0.000000000000000000 ) ) ;
#464=AXIS2_PLACEMENT_3D ( 'NONE', #6114, #639, #2555 ) ;
#471=DIRECTION ( 'NONE',  ( 0.000000000000000000, 1.000000000000000000, 0.000000000000000000 ) ) ;
#601=ORIENTED_EDGE ( 'NONE', *, *, #16837, .F. ) ;
#639=DIRECTION ( 'NONE',  ( -2.269747459788999852E-13, -2.220446049250320181E-15, -1.000000000000000000 ) ) ;
#679=VECTOR ( 'NONE', #9754, 1000.000000000000000 ) ;
#706=DIRECTION ( 'NONE',  ( -6.662161100567945949E-09, 1.000000000000000000, -2.220444537107962377E-15 ) ) ;
#821=ORIENTED_EDGE ( 'NONE', *, *, #18406, .T. ) ;
#857=CONICAL_SURFACE ( 'NONE', #20602, 2.624999999999998668, 0.4636476090008128104 ) ;
#1137=VERTEX_POINT ( 'NONE', #21778 ) ;
#1248=FACE_OUTER_BOUND ( 'NONE', #3520, .T. ) ;
#1514=ORIENTED_EDGE ( 'NONE', *, *, #13472, .F. ) ;
#1577=ORIENTED_EDGE ( 'NONE', *, *, #14549, .T. ) ;
#1605=AXIS2_PLACEMENT_3D ( 'NONE', #402, #3982, #19909 ) ;
#2146=CIRCLE ( 'NONE', #8228, 2.499999999999998668 ) ;
#2160=AXIS2_PLACEMENT_3D ( 'NONE', #7379, #8805, #17825 ) ;
#2187=DIRECTION ( 'NONE',  ( -2.269747459788994803E-13, -2.220446049250320181E-15, -1.000000000000000000 ) ) ;
#2195=DIRECTION ( 'NONE',  ( -6.662161100567945949E-09, 1.000000000000000000, -2.081668171172169697E-15 ) ) ;
#2235=EDGE_CURVE ( 'NONE', #18419, #15816, #7076, .T. ) ;
#2548=EDGE_CURVE ( 'NONE', #15489, #19229, #2146, .T. ) ;
#2555=DIRECTION ( 'NONE',  ( -6.662161563160872600E-09, 1.000000000000000000, -1.982541115402066096E-15 ) ) ;
#2567=EDGE_CURVE ( 'NONE', #9360, #6052, #5928, .T. ) ;
#2569=CARTESIAN_POINT ( 'NONE',  ( 0.000000000000000000, 0.000000000000000000, 0.000000000000000000 ) ) ;
#2634=ORIENTED_EDGE ( 'NONE', *, *, #18406, .F. ) ;
#2768=CARTESIAN_POINT ( 'NONE',  ( -20.00000002229559826, 25.70208919256889857, -8.499999999995555555 ) ) ;
#2782=DIRECTION ( 'NONE',  ( -6.662161563160872600E-09, 1.000000000000000000, -1.982541115402066096E-15 ) ) ;
#2795=CIRCLE ( 'NONE', #14558, 2.749999999999999112 ) ;
#2827=EDGE_LOOP ( 'NONE', ( #21305, #11273, #7669, #7385, #180 ) ) ;
#2869=FACE_OUTER_BOUND ( 'NONE', #8366, .T. ) ;
#2913=DIRECTION ( 'NONE',  ( -6.662160722082822564E-09, 1.000000000000000000, -2.523234146875356491E-15 ) ) ;
#2966=ORIENTED_EDGE ( 'NONE', *, *, #4909, .T. ) ;
#3203=ORIENTED_EDGE ( 'NONE', *, *, #19668, .T. ) ;
#3351=CONICAL_SURFACE ( 'NONE', #12097, 2.624999999999998668, 0.4636476090008101458 ) ;
#3520=EDGE_LOOP ( 'NONE', ( #6079, #3203, #4402, #1577, #1514 ) ) ;
#3600=AXIS2_PLACEMENT_3D ( 'NONE', #18551, #471, #21616 ) ;
#3703=AXIS2_PLACEMENT_3D ( 'NONE', #5629, #21782, #9079 ) ;
#3772=DIRECTION ( 'NONE',  ( 0.000000000000000000, 0.000000000000000000, -1.000000000000000000 ) ) ;
#3982=DIRECTION ( 'NONE',  ( -2.269747459788994803E-13, -2.220446049250320181E-15, -1.000000000000000000 ) ) ;
#4045=SPHERICAL_SURFACE ( 'NONE', #3600, 15.25000000000000000 ) ;
#4140=FACE_OUTER_BOUND ( 'NONE', #19965, .T. ) ;
#4275=ORIENTED_EDGE ( 'NONE', *, *, #16837, .T. ) ;
#4285=AXIS2_PLACEMENT_3D ( 'NONE', #18130, #21552, #12782 ) ;
#4294=FACE_OUTER_BOUND ( 'NONE', #11988, .T. ) ;
#4327=SHAPE_DEFINITION_REPRESENTATION ( #7029, #14436 ) ;
#4342=DIRECTION ( 'NONE',  ( -2.269747459788994803E-13, -2.220446049250320181E-15, -1.000000000000000000 ) ) ;
#4369=UNCERTAINTY_MEASURE_WITH_UNIT (LENGTH_MEASURE( 1.000000000000000082E-05 ), #17141, 'distance_accuracy_value', 'NONE');
#4402=ORIENTED_EDGE ( 'NONE', *, *, #22820, .T. ) ;
#4415=ORIENTED_EDGE ( 'NONE', *, *, #2567, .T. ) ;
#4454=ORIENTED_EDGE ( 'NONE', *, *, #2235, .T. ) ;
#4680=AXIS2_PLACEMENT_3D ( 'NONE', #9067, #14759, #12985 ) ;
#4744=DIRECTION ( 'NONE',  ( -2.269747459788994803E-13, -2.220446049250320181E-15, -1.000000000000000000 ) ) ;
#4768=AXIS2_PLACEMENT_3D ( 'NONE', #320, #20180, #3772 ) ;
#4781=SPHERICAL_SURFACE ( 'NONE', #19037, 15.25000000000000000 ) ;
#4791=DIRECTION ( 'NONE',  ( 2.979206038694609145E-09, -0.4472135954999635343, -0.8944271909999130798 ) ) ;
#4909=EDGE_CURVE ( 'NONE', #5883, #15816, #5673, .T. ) ;
#5173=DESIGN_CONTEXT ( 'detailed design', #6565, 'design' ) ;
#5242=VERTEX_POINT ( 'NONE', #10469 ) ;
#5507=CARTESIAN_POINT ( 'NONE',  ( -22.75000000397123046, 22.95208919256889857, 8.500000000005087486 ) ) ;
#5583=AXIS2_PLACEMENT_3D ( 'NONE', #23352, #19926, #18263 ) ;
#5629=CARTESIAN_POINT ( 'NONE',  ( -20.00000000397450250, 22.95208919256889857, -7.999999999995548450 ) ) ;
#5657=FACE_OUTER_BOUND ( 'NONE', #22187, .T. ) ;
#5673=CIRCLE ( 'NONE', #18964, 15.25000000000000000 ) ;
#5883=VERTEX_POINT ( 'NONE', #5507 ) ;
#5928=CIRCLE ( 'NONE', #13901, 2.749999999999999112 ) ;
#6052=VERTEX_POINT ( 'NONE', #2768 ) ;
#6079=ORIENTED_EDGE ( 'NONE', *, *, #18745, .F. ) ;
#6098=CLOSED_SHELL ( 'NONE', ( #21423, #8761, #13358, #65, #18837, #12707, #14875, #246, #8064, #11318 ) ) ;
#6114=CARTESIAN_POINT ( 'NONE',  ( -20.00000000397459843, 22.95208919256889857, -8.249999999995548450 ) ) ;
#6135=PRODUCT_DEFINITION_FORMATION_WITH_SPECIFIED_SOURCE ( 'ANY', '', #10633, .NOT_KNOWN. ) ;
#6180=AXIS2_PLACEMENT_3D ( 'NONE', #8308, #4744, #21122 ) ;
#6422=ORIENTED_EDGE ( 'NONE', *, *, #20454, .T. ) ;
#6440=MECHANICAL_CONTEXT ( 'NONE', #22918, 'mechanical' ) ;
#6557=CIRCLE ( 'NONE', #1605, 2.749999999999999112 ) ;
#6565=APPLICATION_CONTEXT ( 'configuration controlled 3d designs of mechanical parts and assemblies' ) ;
#6620=DIRECTION ( 'NONE',  ( -6.662161563160872600E-09, 1.000000000000000000, -1.982541115402066096E-15 ) ) ;
#6650=ORIENTED_EDGE ( 'NONE', *, *, #2235, .F. ) ;
#6681=CARTESIAN_POINT ( 'NONE',  ( -20.00000000397270128, 22.95208919256889857, 4.454121720691780225E-12 ) ) ;
#6724=CIRCLE ( 'NONE', #11280, 2.749999999999999112 ) ;
#6795=CYLINDRICAL_SURFACE ( 'NONE', #13189, 2.499999999999998668 ) ;
#6821=CARTESIAN_POINT ( 'NONE',  ( -20.00000000397469790, 22.95208919256889857, -8.499999999995548450 ) ) ;
#7029=PRODUCT_DEFINITION_SHAPE ( 'NONE', 'NONE',  #13725 ) ;
#7076=CIRCLE ( 'NONE', #4768, 15.25000000000000000 ) ;
#7323=CIRCLE ( 'NONE', #20591, 2.499999999999998668 ) ;
#7379=CARTESIAN_POINT ( 'NONE',  ( -20.00000000397129796, 22.95208919256900160, 6.500000000004299672 ) ) ;
#7385=ORIENTED_EDGE ( 'NONE', *, *, #2567, .F. ) ;
#7552=DIRECTION ( 'NONE',  ( -2.269747459788994803E-13, -2.220446049250320181E-15, -1.000000000000000000 ) ) ;
#7669=ORIENTED_EDGE ( 'NONE', *, *, #10647, .T. ) ;
#7790=DIRECTION ( 'NONE',  ( -2.269747459788994803E-13, -2.220446049250325308E-15, -1.000000000000000000 ) ) ;
#7837=ORIENTED_EDGE ( 'NONE', *, *, #10647, .F. ) ;
#7850=CARTESIAN_POINT ( 'NONE',  ( -20.00000000397270128, 22.95208919256889857, 4.454121720691780225E-12 ) ) ;
#8007=( NAMED_UNIT ( * ) SI_UNIT ( $, .STERADIAN. ) SOLID_ANGLE_UNIT ( ) );
#8064=ADVANCED_FACE ( 'NONE', ( #4140 ), #857, .T. ) ;
#8121=ORIENTED_EDGE ( 'NONE', *, *, #12351, .F. ) ;
#8141=DIRECTION ( 'NONE',  ( -6.662161100567945949E-09, 1.000000000000000000, -2.081668171172169697E-15 ) ) ;
#8228=AXIS2_PLACEMENT_3D ( 'NONE', #13359, #2187, #8141 ) ;
#8247=CARTESIAN_POINT ( 'NONE',  ( -19.99999998648642574, 20.32708919256890212, -8.249999999995543121 ) ) ;
#8308=CARTESIAN_POINT ( 'NONE',  ( -20.00000000397469790, 22.95208919256889857, -8.499999999995548450 ) ) ;
#8353=( NAMED_UNIT ( * ) PLANE_ANGLE_UNIT ( ) SI_UNIT ( $, .RADIAN. ) );
#8366=EDGE_LOOP ( 'NONE', ( #21497, #17406, #9181, #10061 ) ) ;
#8562=ORIENTED_EDGE ( 'NONE', *, *, #4909, .F. ) ;
#8687=SPHERICAL_SURFACE ( 'NONE', #2160, 15.25000000000000000 ) ;
#8717=ORIENTED_EDGE ( 'NONE', *, *, #2548, .T. ) ;
#8761=ADVANCED_FACE ( 'NONE', ( #1248 ), #13420, .T. ) ;
#8785=ORIENTED_EDGE ( 'NONE', *, *, #2548, .F. ) ;
#8805=DIRECTION ( 'NONE',  ( 0.000000000000000000, 1.000000000000000000, 0.000000000000000000 ) ) ;
#8980=VERTEX_POINT ( 'NONE', #18007 ) ;
#9024=AXIS2_PLACEMENT_3D ( 'NONE', #20181, #22944, #14483 ) ;
#9067=CARTESIAN_POINT ( 'NONE',  ( -20.00000000397129796, 22.95208919256900160, 6.500000000004299672 ) ) ;
#9079=DIRECTION ( 'NONE',  ( -6.662161100567945949E-09, 1.000000000000000000, -2.081668171172169697E-15 ) ) ;
#9181=ORIENTED_EDGE ( 'NONE', *, *, #18606, .T. ) ;
#9343=EDGE_CURVE ( 'NONE', #19229, #20796, #17274, .T. ) ;
#9360=VERTEX_POINT ( 'NONE', #10508 ) ;
#9362=DIRECTION ( 'NONE',  ( 2.979611953927833651E-09, -0.4472135954999619800, 0.8944271909999139680 ) ) ;
#9480=CARTESIAN_POINT ( 'NONE',  ( -19.99999998648272737, 20.32708919256900160, 8.250000000004465761 ) ) ;
#9508=DIRECTION ( 'NONE',  ( 1.224646799147353207E-16, 1.000000000000000000, -0.000000000000000000 ) ) ;
#9581=LINE ( 'NONE', #15262, #9983 ) ;
#9611=DIRECTION ( 'NONE',  ( -6.662160722082822564E-09, 1.000000000000000000, -2.523234146875356491E-15 ) ) ;
#9651=ORIENTED_EDGE ( 'NONE', *, *, #18606, .F. ) ;
#9754=DIRECTION ( 'NONE',  ( -2.269747459788994803E-13, -2.220446049250325308E-15, -1.000000000000000000 ) ) ;
#9817=ORIENTED_EDGE ( 'NONE', *, *, #11707, .T. ) ;
#9876=CYLINDRICAL_SURFACE ( 'NONE', #10511, 2.499999999999998668 ) ;
#9965=CARTESIAN_POINT ( 'NONE',  ( -20.00000000397080058, 22.95208919256900160, 8.500000000004460432 ) ) ;
#9982=CIRCLE ( 'NONE', #4285, 15.25000000000000000 ) ;
#9983=VECTOR ( 'NONE', #7790, 1000.000000000000000 ) ;
#10026=DIRECTION ( 'NONE',  ( -2.269747459788994803E-13, -2.220446049250325308E-15, -1.000000000000000000 ) ) ;
#10061=ORIENTED_EDGE ( 'NONE', *, *, #10830, .T. ) ;
#10066=CARTESIAN_POINT ( 'NONE',  ( -20.00000000397080058, 22.95208919256900160, 8.500000000004460432 ) ) ;
#10314=ORIENTED_EDGE ( 'NONE', *, *, #18745, .T. ) ;
#10355=CONICAL_SURFACE ( 'NONE', #464, 2.624999999999998668, 0.4636476090008101458 ) ;
#10392=DIRECTION ( 'NONE',  ( -2.269747459788994803E-13, -2.220446049250320181E-15, -1.000000000000000000 ) ) ;
#10467=ORIENTED_EDGE ( 'NONE', *, *, #22742, .F. ) ;
#10469=CARTESIAN_POINT ( 'NONE',  ( -19.99999998648272737, 20.45208919256900160, 8.000000000004465761 ) ) ;
#10508=CARTESIAN_POINT ( 'NONE',  ( -22.75000000397511002, 22.95208919256900160, -8.499999999994924949 ) ) ;
#10511=AXIS2_PLACEMENT_3D ( 'NONE', #7850, #16988, #706 ) ;
#10633=PRODUCT ( '1602p_c_19', '1602p_c_19', '', ( #6440 ) ) ;
#10634=ORIENTED_EDGE ( 'NONE', *, *, #22107, .T. ) ;
#10645=VECTOR ( 'NONE', #4791, 1000.000000000000114 ) ;
#10647=EDGE_CURVE ( 'NONE', #15489, #6052, #19062, .T. ) ;
#10736=FACE_OUTER_BOUND ( 'NONE', #13269, .T. ) ;
#10792=CARTESIAN_POINT ( 'NONE',  ( -20.00000000397090005, 22.95208919256900160, 8.000000000004460432 ) ) ;
#10830=EDGE_CURVE ( 'NONE', #20796, #9360, #12416, .T. ) ;
#11247=( GEOMETRIC_REPRESENTATION_CONTEXT ( 3 ) GLOBAL_UNCERTAINTY_ASSIGNED_CONTEXT ( ( #4369 ) ) GLOBAL_UNIT_ASSIGNED_CONTEXT ( ( #17141, #8353, #8007 ) ) REPRESENTATION_CONTEXT ( 'NONE', 'WORKASPACE' ) );
#11273=ORIENTED_EDGE ( 'NONE', *, *, #12351, .T. ) ;
#11280=AXIS2_PLACEMENT_3D ( 'NONE', #10066, #11623, #2913 ) ;
#11318=ADVANCED_FACE ( 'NONE', ( #19031 ), #6795, .T. ) ;
#11392=DIRECTION ( 'NONE',  ( -2.269747459788994803E-13, -2.220446049250320181E-15, -1.000000000000000000 ) ) ;
#11410=CARTESIAN_POINT ( 'NONE',  ( -20.00000000397090005, 22.95208919256900160, 8.250000000004460432 ) ) ;
#11558=DIRECTION ( 'NONE',  ( -1.000000000000000000, 2.275047181608927151E-16, 0.000000000000000000 ) ) ;
#11623=DIRECTION ( 'NONE',  ( -2.269747459788994803E-13, -2.220446049250320181E-15, -1.000000000000000000 ) ) ;
#11693=ORIENTED_EDGE ( 'NONE', *, *, #13472, .T. ) ;
#11707=EDGE_CURVE ( 'NONE', #11832, #15489, #18888, .T. ) ;
#11832=VERTEX_POINT ( 'NONE', #15783 ) ;
#11957=CARTESIAN_POINT ( 'NONE',  ( -20.00000000397420052, 22.95208919256889857, 8.750000000004618528 ) ) ;
#11980=AXIS2_PLACEMENT_3D ( 'NONE', #15904, #10392, #19829 ) ;
#11988=EDGE_LOOP ( 'NONE', ( #13974, #6422, #8785, #21582 ) ) ;
#12097=AXIS2_PLACEMENT_3D ( 'NONE', #22591, #13579, #2782 ) ;
#12238=CARTESIAN_POINT ( 'NONE',  ( -20.00000002062990490, 25.45208919256889857, -7.999999999995553779 ) ) ;
#12346=EDGE_LOOP ( 'NONE', ( #8562, #13383, #2634, #4454 ) ) ;
#12351=EDGE_CURVE ( 'NONE', #19229, #15489, #13954, .T. ) ;
#12352=CIRCLE ( 'NONE', #11980, 2.749999999999999112 ) ;
#12416=CIRCLE ( 'NONE', #19606, 2.749999999999999112 ) ;
#12707=ADVANCED_FACE ( 'NONE', ( #15832 ), #3351, .T. ) ;
#12739=AXIS2_PLACEMENT_3D ( 'NONE', #2569, #13380, #415 ) ;
#12782=DIRECTION ( 'NONE',  ( -1.000000000000000000, 2.275047181608927151E-16, 0.000000000000000000 ) ) ;
#12970=CARTESIAN_POINT ( 'NONE',  ( -20.00000000397080058, 22.95208919256900160, 8.500000000004460432 ) ) ;
#12985=DIRECTION ( 'NONE',  ( 0.000000000000000000, 0.000000000000000000, -1.000000000000000000 ) ) ;
#13189=AXIS2_PLACEMENT_3D ( 'NONE', #6681, #10026, #14026 ) ;
#13264=CARTESIAN_POINT ( 'NONE',  ( -20.00000002145907274, 25.57708919256899804, 8.250000000004455103 ) ) ;
#13269=EDGE_LOOP ( 'NONE', ( #14927, #18125, #4415, #4275 ) ) ;
#13358=ADVANCED_FACE ( 'NONE', ( #5657 ), #20281, .T. ) ;
#13359=CARTESIAN_POINT ( 'NONE',  ( -20.00000000397450250, 22.95208919256889857, -7.999999999995548450 ) ) ;
#13380=DIRECTION ( 'NONE',  ( 0.000000000000000000, 0.000000000000000000, 1.000000000000000000 ) ) ;
#13383=ORIENTED_EDGE ( 'NONE', *, *, #22820, .F. ) ;
#13420=CONICAL_SURFACE ( 'NONE', #21378, 2.624999999999998668, 0.4636476090008128104 ) ;
#13472=EDGE_CURVE ( 'NONE', #11832, #16045, #18500, .T. ) ;
#13579=DIRECTION ( 'NONE',  ( -2.269747459788999852E-13, -2.220446049250320181E-15, -1.000000000000000000 ) ) ;
#13725=PRODUCT_DEFINITION ( 'UNKNOWN', '', #6135, #5173 ) ;
#13824=SHAPE_REPRESENTATION_RELATIONSHIP ( 'NONE' , 'NONE' ,  #14436, #20135 ) ;
#13901=AXIS2_PLACEMENT_3D ( 'NONE', #20474, #4342, #18833 ) ;
#13954=CIRCLE ( 'NONE', #3703, 2.499999999999998668 ) ;
#13974=ORIENTED_EDGE ( 'NONE', *, *, #22742, .T. ) ;
#14026=DIRECTION ( 'NONE',  ( -6.662161100567945949E-09, 1.000000000000000000, -2.220444537107962377E-15 ) ) ;
#14342=ORIENTED_EDGE ( 'NONE', *, *, #9343, .T. ) ;
#14436=SHAPE_REPRESENTATION ( '1602p_c_19', ( #12739 ), #11247 ) ;
#14483=DIRECTION ( 'NONE',  ( -6.662161100567945949E-09, 1.000000000000000000, -2.081668171172169697E-15 ) ) ;
#14549=EDGE_CURVE ( 'NONE', #5883, #16045, #15051, .T. ) ;
#14558=AXIS2_PLACEMENT_3D ( 'NONE', #9965, #11392, #9611 ) ;
#14753=CARTESIAN_POINT ( 'NONE',  ( -20.00000002229178619, 25.70208919256900160, 8.500000000004453327 ) ) ;
#14759=DIRECTION ( 'NONE',  ( 0.000000000000000000, -1.000000000000000000, 0.000000000000000000 ) ) ;
#14840=CARTESIAN_POINT ( 'NONE',  ( -20.00000000397420052, 22.95208919256889857, -6.499999999995379696 ) ) ;
#14875=ADVANCED_FACE ( 'NONE', ( #2869 ), #8687, .T. ) ;
#14901=DIRECTION ( 'NONE',  ( -2.979612008695687415E-09, 0.4472135954999595375, -0.8944271909999150783 ) ) ;
#14904=CIRCLE ( 'NONE', #6180, 2.749999999999999112 ) ;
#14927=ORIENTED_EDGE ( 'NONE', *, *, #19277, .F. ) ;
#15013=CARTESIAN_POINT ( 'NONE',  ( -20.00000002146277467, 25.57708919256889857, -8.249999999995553779 ) ) ;
#15051=CIRCLE ( 'NONE', #22617, 2.749999999999999112 ) ;
#15116=VECTOR ( 'NONE', #22159, 1000.000000000000000 ) ;
#15262=CARTESIAN_POINT ( 'NONE',  ( -19.99999998731729889, 20.45208919256890212, 4.459672832034550052E-12 ) ) ;
#15489=VERTEX_POINT ( 'NONE', #12238 ) ;
#15783=CARTESIAN_POINT ( 'NONE',  ( -20.00000002062630244, 25.45208919256899804, 8.000000000004455103 ) ) ;
#15816=VERTEX_POINT ( 'NONE', #11957 ) ;
#15832=FACE_OUTER_BOUND ( 'NONE', #2827, .T. ) ;
#15904=CARTESIAN_POINT ( 'NONE',  ( -20.00000000397080058, 22.95208919256900160, 8.500000000004460432 ) ) ;
#16045=VERTEX_POINT ( 'NONE', #14753 ) ;
#16124=ORIENTED_EDGE ( 'NONE', *, *, #20454, .F. ) ;
#16166=CARTESIAN_POINT ( 'NONE',  ( -20.00000000397129796, 22.95208919256900160, 6.500000000004299672 ) ) ;
#16326=VERTEX_POINT ( 'NONE', #22930 ) ;
#16837=EDGE_CURVE ( 'NONE', #6052, #8980, #14904, .T. ) ;
#16972=CARTESIAN_POINT ( 'NONE',  ( -20.00000002062810367, 25.45208919256889857, 4.448570609349010398E-12 ) ) ;
#16988=DIRECTION ( 'NONE',  ( -2.269747459788994803E-13, -2.220446049250325308E-15, -1.000000000000000000 ) ) ;
#17141=( LENGTH_UNIT ( ) NAMED_UNIT ( * ) SI_UNIT ( .MILLI., .METRE. ) );
#17187=MANIFOLD_SOLID_BREP ( 'Imported1', #6098 ) ;
#17210=VECTOR ( 'NONE', #9362, 999.9999999999998863 ) ;
#17274=LINE ( 'NONE', #8247, #10645 ) ;
#17406=ORIENTED_EDGE ( 'NONE', *, *, #19277, .T. ) ;
#17633=DIRECTION ( 'NONE',  ( -2.269747459788994803E-13, -2.220446049250320181E-15, -1.000000000000000000 ) ) ;
#17730=DIRECTION ( 'NONE',  ( 1.000000000000000000, 0.000000000000000000, 0.000000000000000000 ) ) ;
#17825=DIRECTION ( 'NONE',  ( 1.000000000000000000, 0.000000000000000000, 0.000000000000000000 ) ) ;
#17966=LINE ( 'NONE', #9480, #17210 ) ;
#18007=CARTESIAN_POINT ( 'NONE',  ( -17.25000000397428934, 22.95208919256900160, -8.499999999996171951 ) ) ;
#18125=ORIENTED_EDGE ( 'NONE', *, *, #18631, .T. ) ;
#18130=CARTESIAN_POINT ( 'NONE',  ( -20.00000000397129796, 22.95208919256900160, 6.500000000004299672 ) ) ;
#18176=EDGE_LOOP ( 'NONE', ( #8717, #14342, #9651, #601, #7837 ) ) ;
#18263=DIRECTION ( 'NONE',  ( 1.000000000000000000, 0.000000000000000000, 0.000000000000000000 ) ) ;
#18406=EDGE_CURVE ( 'NONE', #18419, #1137, #2795, .T. ) ;
#18419=VERTEX_POINT ( 'NONE', #23225 ) ;
#18435=FACE_OUTER_BOUND ( 'NONE', #12346, .T. ) ;
#18448=DIRECTION ( 'NONE',  ( -2.269747459788994803E-13, -2.220446049250320181E-15, -1.000000000000000000 ) ) ;
#18500=LINE ( 'NONE', #13264, #15116 ) ;
#18551=CARTESIAN_POINT ( 'NONE',  ( -20.00000000397420052, 22.95208919256889857, -6.499999999995379696 ) ) ;
#18601=FACE_OUTER_BOUND ( 'NONE', #18176, .T. ) ;
#18606=EDGE_CURVE ( 'NONE', #8980, #20796, #6557, .T. ) ;
#18631=EDGE_CURVE ( 'NONE', #16326, #9360, #9982, .T. ) ;
#18745=EDGE_CURVE ( 'NONE', #5242, #11832, #7323, .T. ) ;
#18803=DIRECTION ( 'NONE',  ( -6.662160722082822564E-09, 1.000000000000000000, -2.523234146875356491E-15 ) ) ;
#18833=DIRECTION ( 'NONE',  ( -6.662160722082822564E-09, 1.000000000000000000, -2.523234146875356491E-15 ) ) ;
#18837=ADVANCED_FACE ( 'NONE', ( #18601 ), #10355, .T. ) ;
#18888=LINE ( 'NONE', #16972, #679 ) ;
#18964=AXIS2_PLACEMENT_3D ( 'NONE', #14840, #9508, #11558 ) ;
#19031=FACE_OUTER_BOUND ( 'NONE', #21809, .T. ) ;
#19037=AXIS2_PLACEMENT_3D ( 'NONE', #16166, #21160, #17730 ) ;
#19062=LINE ( 'NONE', #15013, #26 ) ;
#19179=DIRECTION ( 'NONE',  ( -6.662160722082822564E-09, 1.000000000000000000, -2.523234146875356491E-15 ) ) ;
#19229=VERTEX_POINT ( 'NONE', #21773 ) ;
#19261=CIRCLE ( 'NONE', #9024, 2.499999999999998668 ) ;
#19277=EDGE_CURVE ( 'NONE', #16326, #8980, #19458, .T. ) ;
#19458=CIRCLE ( 'NONE', #4680, 15.25000000000000000 ) ;
#19606=AXIS2_PLACEMENT_3D ( 'NONE', #6821, #17633, #19179 ) ;
#19668=EDGE_CURVE ( 'NONE', #5242, #1137, #17966, .T. ) ;
#19829=DIRECTION ( 'NONE',  ( -6.662160722082822564E-09, 1.000000000000000000, -2.523234146875356491E-15 ) ) ;
#19909=DIRECTION ( 'NONE',  ( -6.662160722082822564E-09, 1.000000000000000000, -2.523234146875356491E-15 ) ) ;
#19926=DIRECTION ( 'NONE',  ( 0.000000000000000000, 1.000000000000000000, 0.000000000000000000 ) ) ;
#19965=EDGE_LOOP ( 'NONE', ( #21463, #10467, #11693, #10634, #821 ) ) ;
#20135=ADVANCED_BREP_SHAPE_REPRESENTATION ( '', ( #17187, #12739 ), #11247 ) ;
#20180=DIRECTION ( 'NONE',  ( 0.000000000000000000, -1.000000000000000000, 0.000000000000000000 ) ) ;
#20181=CARTESIAN_POINT ( 'NONE',  ( -20.00000000397090005, 22.95208919256900160, 8.000000000004460432 ) ) ;
#20281=SPHERICAL_SURFACE ( 'NONE', #5583, 15.25000000000000000 ) ;
#20454=EDGE_CURVE ( 'NONE', #5242, #19229, #9581, .T. ) ;
#20474=CARTESIAN_POINT ( 'NONE',  ( -20.00000000397469790, 22.95208919256889857, -8.499999999995548450 ) ) ;
#20527=DIRECTION ( 'NONE',  ( -6.662161563160872600E-09, 1.000000000000000000, -1.982541115402066096E-15 ) ) ;
#20591=AXIS2_PLACEMENT_3D ( 'NONE', #10792, #7552, #2195 ) ;
#20602=AXIS2_PLACEMENT_3D ( 'NONE', #11410, #22539, #20527 ) ;
#20796=VERTEX_POINT ( 'NONE', #260 ) ;
#21122=DIRECTION ( 'NONE',  ( -6.662160722082822564E-09, 1.000000000000000000, -2.523234146875356491E-15 ) ) ;
#21160=DIRECTION ( 'NONE',  ( 0.000000000000000000, 1.000000000000000000, 0.000000000000000000 ) ) ;
#21197=CARTESIAN_POINT ( 'NONE',  ( -20.00000000397090005, 22.95208919256900160, 8.250000000004460432 ) ) ;
#21305=ORIENTED_EDGE ( 'NONE', *, *, #9343, .F. ) ;
#21378=AXIS2_PLACEMENT_3D ( 'NONE', #21197, #22973, #6620 ) ;
#21423=ADVANCED_FACE ( 'NONE', ( #4294 ), #9876, .T. ) ;
#21463=ORIENTED_EDGE ( 'NONE', *, *, #19668, .F. ) ;
#21491=ORIENTED_EDGE ( 'NONE', *, *, #22107, .F. ) ;
#21497=ORIENTED_EDGE ( 'NONE', *, *, #18631, .F. ) ;
#21552=DIRECTION ( 'NONE',  ( 1.224646799147353207E-16, 1.000000000000000000, -0.000000000000000000 ) ) ;
#21582=ORIENTED_EDGE ( 'NONE', *, *, #11707, .F. ) ;
#21616=DIRECTION ( 'NONE',  ( 1.000000000000000000, 0.000000000000000000, 0.000000000000000000 ) ) ;
#21773=CARTESIAN_POINT ( 'NONE',  ( -19.99999998648642574, 20.45208919256890212, -7.999999999995544009 ) ) ;
#21778=CARTESIAN_POINT ( 'NONE',  ( -19.99999998564990022, 20.20208919256900160, 8.500000000004467537 ) ) ;
#21782=DIRECTION ( 'NONE',  ( -2.269747459788994803E-13, -2.220446049250320181E-15, -1.000000000000000000 ) ) ;
#21809=EDGE_LOOP ( 'NONE', ( #16124, #10314, #9817, #8121 ) ) ;
#22107=EDGE_CURVE ( 'NONE', #16045, #18419, #6724, .T. ) ;
#22111=ORIENTED_EDGE ( 'NONE', *, *, #14549, .F. ) ;
#22159=DIRECTION ( 'NONE',  ( -2.979205983926755381E-09, 0.4472135954999659213, 0.8944271909999118586 ) ) ;
#22187=EDGE_LOOP ( 'NONE', ( #22111, #2966, #6650, #21491 ) ) ;
#22539=DIRECTION ( 'NONE',  ( 2.269747459788999852E-13, 2.220446049250325308E-15, 1.000000000000000000 ) ) ;
#22591=CARTESIAN_POINT ( 'NONE',  ( -20.00000000397459843, 22.95208919256889857, -8.249999999995548450 ) ) ;
#22617=AXIS2_PLACEMENT_3D ( 'NONE', #12970, #18448, #18803 ) ;
#22742=EDGE_CURVE ( 'NONE', #11832, #5242, #19261, .T. ) ;
#22820=EDGE_CURVE ( 'NONE', #1137, #5883, #12352, .T. ) ;
#22918=APPLICATION_CONTEXT ( 'configuration controlled 3d designs of mechanical parts and assemblies' ) ;
#22930=CARTESIAN_POINT ( 'NONE',  ( -20.00000000397129796, 22.95208919256900160, -8.749999999995699440 ) ) ;
#22944=DIRECTION ( 'NONE',  ( -2.269747459788994803E-13, -2.220446049250320181E-15, -1.000000000000000000 ) ) ;
#22973=DIRECTION ( 'NONE',  ( 2.269747459788999852E-13, 2.220446049250325308E-15, 1.000000000000000000 ) ) ;
#23225=CARTESIAN_POINT ( 'NONE',  ( -17.25000000397036715, 22.95208919256889857, 8.500000000003836931 ) ) ;
#23352=CARTESIAN_POINT ( 'NONE',  ( -20.00000000397420052, 22.95208919256889857, -6.499999999995379696 ) ) ;
#23522=COLOUR_RGB('Light Blue', 0.66274510, 0.83137255, 0.94901961);
#23523=FILL_AREA_STYLE_COLOUR('',#23522);
#23524=FILL_AREA_STYLE('',(#23523));
#23525=SURFACE_STYLE_FILL_AREA(#23524);
#23526=SURFACE_SIDE_STYLE('',(#23525));
#23527=SURFACE_STYLE_USAGE(.BOTH.,#23526);
#23528=PRESENTATION_STYLE_ASSIGNMENT((#23527));
#23623=STYLED_ITEM('',(#23528),#17187);
#23624=MECHANICAL_DESIGN_GEOMETRIC_PRESENTATION_REPRESENTATION('',(#23623),#11247);
ENDSEC;
END-ISO-10303-21;
